ISO-10303-21;
HEADER;
/* Generated by software containing ST-Developer
 * from STEP Tools, Inc. (www.steptools.com) 
 */

FILE_DESCRIPTION(
/* description */ ('Counterbalanced vertical column'),
/* implementation_level */ '2;1');

FILE_NAME(
/* name */ 'Captive slot nut.step',
/* time_stamp */ '2026-10-29T16:47:22-07:00',
/* author */ (''),
/* organization */ (''),
/* preprocessor_version */ 'ST-DEVELOPER v20.2',
/* originating_system */ 'Autodesk Translation Framework v15.17.0.0',
/* authorisation */ '');

FILE_SCHEMA (('AUTOMOTIVE_DESIGN { 1 0 10303 214 3 1 1 }'));
ENDSEC;

DATA;
#10=MECHANICAL_DESIGN_GEOMETRIC_PRESENTATION_REPRESENTATION('',(#371),#15040);
#276=ELLIPSE('',#7910,0.299389011154384,0.2117);
#277=ELLIPSE('',#7914,0.299389011154384,0.2117);
#301=SHAPE_REPRESENTATION_RELATIONSHIP('SRR','None',#15205,#336);
#336=ADVANCED_BREP_SHAPE_REPRESENTATION('',(#404),#15024);
#371=STYLED_ITEM('',(#15464),#404);
#404=MANIFOLD_SOLID_BREP('Body1',#7096);
#495=FACE_BOUND('',#1557,.T.);
#706=PLANE('',#7900);
#707=PLANE('',#7901);
#708=PLANE('',#7902);
#709=PLANE('',#7904);
#710=PLANE('',#7905);
#711=PLANE('',#7906);
#712=PLANE('',#7907);
#713=PLANE('',#7908);
#714=PLANE('',#7909);
#715=PLANE('',#7916);
#716=PLANE('',#7917);
#717=PLANE('',#7918);
#718=PLANE('',#7919);
#1070=FACE_OUTER_BOUND('',#1554,.T.);
#1071=FACE_OUTER_BOUND('',#1555,.T.);
#1072=FACE_OUTER_BOUND('',#1556,.T.);
#1073=FACE_OUTER_BOUND('',#1558,.T.);
#1074=FACE_OUTER_BOUND('',#1559,.T.);
#1075=FACE_OUTER_BOUND('',#1560,.T.);
#1076=FACE_OUTER_BOUND('',#1561,.T.);
#1077=FACE_OUTER_BOUND('',#1562,.T.);
#1078=FACE_OUTER_BOUND('',#1563,.T.);
#1079=FACE_OUTER_BOUND('',#1564,.T.);
#1080=FACE_OUTER_BOUND('',#1565,.T.);
#1081=FACE_OUTER_BOUND('',#1566,.T.);
#1082=FACE_OUTER_BOUND('',#1567,.T.);
#1083=FACE_OUTER_BOUND('',#1568,.T.);
#1554=EDGE_LOOP('',(#5836,#5837,#5838,#5839));
#1555=EDGE_LOOP('',(#5840,#5841,#5842,#5843));
#1556=EDGE_LOOP('',(#5844,#5845,#5846,#5847));
#1557=EDGE_LOOP('',(#5848));
#1558=EDGE_LOOP('',(#5849,#5850,#5851,#5852,#5853,#5854,#5855,#5856,#5857,
#5858));
#1559=EDGE_LOOP('',(#5859,#5860,#5861,#5862));
#1560=EDGE_LOOP('',(#5863,#5864,#5865,#5866));
#1561=EDGE_LOOP('',(#5867,#5868,#5869,#5870,#5871,#5872,#5873,#5874,#5875,
#5876));
#1562=EDGE_LOOP('',(#5877,#5878,#5879,#5880));
#1563=EDGE_LOOP('',(#5881,#5882,#5883,#5884,#5885,#5886));
#1564=EDGE_LOOP('',(#5887,#5888,#5889,#5890,#5891,#5892,#5893,#5894));
#1565=EDGE_LOOP('',(#5895,#5896,#5897,#5898,#5899));
#1566=EDGE_LOOP('',(#5900,#5901,#5902,#5903));
#1567=EDGE_LOOP('',(#5904,#5905,#5906,#5907,#5908,#5909));
#1568=EDGE_LOOP('',(#5910,#5911,#5912,#5913));
#2139=LINE('',#14118,#2810);
#2140=LINE('',#14120,#2811);
#2141=LINE('',#14122,#2812);
#2142=LINE('',#14123,#2813);
#2143=LINE('',#14126,#2814);
#2144=LINE('',#14128,#2815);
#2145=LINE('',#14129,#2816);
#2146=LINE('',#14132,#2817);
#2147=LINE('',#14134,#2818);
#2148=LINE('',#14135,#2819);
#2149=LINE('',#14140,#2820);
#2150=LINE('',#14142,#2821);
#2151=LINE('',#14144,#2822);
#2152=LINE('',#14146,#2823);
#2153=LINE('',#14148,#2824);
#2154=LINE('',#14150,#2825);
#2155=LINE('',#14151,#2826);
#2156=LINE('',#14154,#2827);
#2157=LINE('',#14155,#2828);
#2158=LINE('',#14158,#2829);
#2159=LINE('',#14159,#2830);
#2160=LINE('',#14162,#2831);
#2161=LINE('',#14164,#2832);
#2162=LINE('',#14166,#2833);
#2163=LINE('',#14168,#2834);
#2164=LINE('',#14169,#2835);
#2165=LINE('',#14171,#2836);
#2166=LINE('',#14174,#2837);
#2167=LINE('',#14177,#2838);
#2168=LINE('',#14181,#2839);
#2169=LINE('',#14188,#2840);
#2170=LINE('',#14190,#2841);
#2171=LINE('',#14192,#2842);
#2810=VECTOR('',#9415,1.);
#2811=VECTOR('',#9416,1.);
#2812=VECTOR('',#9417,1.);
#2813=VECTOR('',#9418,1.);
#2814=VECTOR('',#9421,1.);
#2815=VECTOR('',#9422,1.);
#2816=VECTOR('',#9423,1.);
#2817=VECTOR('',#9426,1.);
#2818=VECTOR('',#9427,1.);
#2819=VECTOR('',#9428,1.);
#2820=VECTOR('',#9433,1.);
#2821=VECTOR('',#9434,1.);
#2822=VECTOR('',#9435,1.);
#2823=VECTOR('',#9436,1.);
#2824=VECTOR('',#9437,1.);
#2825=VECTOR('',#9438,1.);
#2826=VECTOR('',#9439,1.);
#2827=VECTOR('',#9442,1.);
#2828=VECTOR('',#9443,1.);
#2829=VECTOR('',#9446,1.);
#2830=VECTOR('',#9447,1.);
#2831=VECTOR('',#9450,1.);
#2832=VECTOR('',#9451,1.);
#2833=VECTOR('',#9452,1.);
#2834=VECTOR('',#9453,1.);
#2835=VECTOR('',#9454,1.);
#2836=VECTOR('',#9457,1.);
#2837=VECTOR('',#9460,1.);
#2838=VECTOR('',#9463,1.);
#2839=VECTOR('',#9468,0.21);
#2840=VECTOR('',#9477,1.);
#2841=VECTOR('',#9480,1.);
#2842=VECTOR('',#9483,1.);
#3222=CIRCLE('',#7903,0.2117);
#3223=CIRCLE('',#7912,0.2117);
#3224=CIRCLE('',#7913,0.2117);
#3225=CIRCLE('',#7915,0.2117);
#3653=VERTEX_POINT('',#14116);
#3654=VERTEX_POINT('',#14117);
#3655=VERTEX_POINT('',#14119);
#3656=VERTEX_POINT('',#14121);
#3657=VERTEX_POINT('',#14125);
#3658=VERTEX_POINT('',#14127);
#3659=VERTEX_POINT('',#14131);
#3660=VERTEX_POINT('',#14133);
#3661=VERTEX_POINT('',#14136);
#3662=VERTEX_POINT('',#14139);
#3663=VERTEX_POINT('',#14141);
#3664=VERTEX_POINT('',#14143);
#3665=VERTEX_POINT('',#14145);
#3666=VERTEX_POINT('',#14147);
#3667=VERTEX_POINT('',#14149);
#3668=VERTEX_POINT('',#14153);
#3669=VERTEX_POINT('',#14157);
#3670=VERTEX_POINT('',#14161);
#3671=VERTEX_POINT('',#14163);
#3672=VERTEX_POINT('',#14165);
#3673=VERTEX_POINT('',#14167);
#3674=VERTEX_POINT('',#14173);
#3675=VERTEX_POINT('',#14175);
#3676=VERTEX_POINT('',#14179);
#3677=VERTEX_POINT('',#14182);
#3678=VERTEX_POINT('',#14184);
#4419=EDGE_CURVE('',#3653,#3654,#2139,.T.);
#4420=EDGE_CURVE('',#3655,#3653,#2140,.T.);
#4421=EDGE_CURVE('',#3656,#3655,#2141,.T.);
#4422=EDGE_CURVE('',#3654,#3656,#2142,.T.);
#4423=EDGE_CURVE('',#3655,#3657,#2143,.T.);
#4424=EDGE_CURVE('',#3658,#3657,#2144,.T.);
#4425=EDGE_CURVE('',#3656,#3658,#2145,.T.);
#4426=EDGE_CURVE('',#3657,#3659,#2146,.T.);
#4427=EDGE_CURVE('',#3659,#3660,#2147,.T.);
#4428=EDGE_CURVE('',#3660,#3658,#2148,.T.);
#4429=EDGE_CURVE('',#3661,#3661,#3222,.T.);
#4430=EDGE_CURVE('',#3662,#3653,#2149,.T.);
#4431=EDGE_CURVE('',#3663,#3662,#2150,.T.);
#4432=EDGE_CURVE('',#3663,#3664,#2151,.T.);
#4433=EDGE_CURVE('',#3665,#3664,#2152,.T.);
#4434=EDGE_CURVE('',#3665,#3666,#2153,.T.);
#4435=EDGE_CURVE('',#3666,#3667,#2154,.T.);
#4436=EDGE_CURVE('',#3667,#3659,#2155,.T.);
#4437=EDGE_CURVE('',#3667,#3668,#2156,.T.);
#4438=EDGE_CURVE('',#3668,#3660,#2157,.T.);
#4439=EDGE_CURVE('',#3669,#3666,#2158,.T.);
#4440=EDGE_CURVE('',#3668,#3669,#2159,.T.);
#4441=EDGE_CURVE('',#3670,#3669,#2160,.T.);
#4442=EDGE_CURVE('',#3671,#3670,#2161,.T.);
#4443=EDGE_CURVE('',#3671,#3672,#2162,.T.);
#4444=EDGE_CURVE('',#3673,#3672,#2163,.T.);
#4445=EDGE_CURVE('',#3673,#3654,#2164,.T.);
#4446=EDGE_CURVE('',#3670,#3665,#2165,.T.);
#4447=EDGE_CURVE('',#3664,#3674,#2166,.T.);
#4448=EDGE_CURVE('',#3674,#3675,#276,.T.);
#4449=EDGE_CURVE('',#3675,#3671,#2167,.T.);
#4450=EDGE_CURVE('',#3676,#3674,#3223,.F.);
#4451=EDGE_CURVE('',#3676,#3661,#2168,.T.);
#4452=EDGE_CURVE('',#3677,#3676,#3224,.F.);
#4453=EDGE_CURVE('',#3678,#3677,#277,.T.);
#4454=EDGE_CURVE('',#3675,#3678,#3225,.F.);
#4455=EDGE_CURVE('',#3677,#3663,#2169,.T.);
#4456=EDGE_CURVE('',#3672,#3678,#2170,.T.);
#4457=EDGE_CURVE('',#3662,#3673,#2171,.T.);
#5836=ORIENTED_EDGE('',*,*,#4419,.F.);
#5837=ORIENTED_EDGE('',*,*,#4420,.F.);
#5838=ORIENTED_EDGE('',*,*,#4421,.F.);
#5839=ORIENTED_EDGE('',*,*,#4422,.F.);
#5840=ORIENTED_EDGE('',*,*,#4421,.T.);
#5841=ORIENTED_EDGE('',*,*,#4423,.T.);
#5842=ORIENTED_EDGE('',*,*,#4424,.F.);
#5843=ORIENTED_EDGE('',*,*,#4425,.F.);
#5844=ORIENTED_EDGE('',*,*,#4426,.T.);
#5845=ORIENTED_EDGE('',*,*,#4427,.T.);
#5846=ORIENTED_EDGE('',*,*,#4428,.T.);
#5847=ORIENTED_EDGE('',*,*,#4424,.T.);
#5848=ORIENTED_EDGE('',*,*,#4429,.T.);
#5849=ORIENTED_EDGE('',*,*,#4426,.F.);
#5850=ORIENTED_EDGE('',*,*,#4423,.F.);
#5851=ORIENTED_EDGE('',*,*,#4420,.T.);
#5852=ORIENTED_EDGE('',*,*,#4430,.F.);
#5853=ORIENTED_EDGE('',*,*,#4431,.F.);
#5854=ORIENTED_EDGE('',*,*,#4432,.T.);
#5855=ORIENTED_EDGE('',*,*,#4433,.F.);
#5856=ORIENTED_EDGE('',*,*,#4434,.T.);
#5857=ORIENTED_EDGE('',*,*,#4435,.T.);
#5858=ORIENTED_EDGE('',*,*,#4436,.T.);
#5859=ORIENTED_EDGE('',*,*,#4437,.T.);
#5860=ORIENTED_EDGE('',*,*,#4438,.T.);
#5861=ORIENTED_EDGE('',*,*,#4427,.F.);
#5862=ORIENTED_EDGE('',*,*,#4436,.F.);
#5863=ORIENTED_EDGE('',*,*,#4439,.F.);
#5864=ORIENTED_EDGE('',*,*,#4440,.F.);
#5865=ORIENTED_EDGE('',*,*,#4437,.F.);
#5866=ORIENTED_EDGE('',*,*,#4435,.F.);
#5867=ORIENTED_EDGE('',*,*,#4428,.F.);
#5868=ORIENTED_EDGE('',*,*,#4438,.F.);
#5869=ORIENTED_EDGE('',*,*,#4440,.T.);
#5870=ORIENTED_EDGE('',*,*,#4441,.F.);
#5871=ORIENTED_EDGE('',*,*,#4442,.F.);
#5872=ORIENTED_EDGE('',*,*,#4443,.T.);
#5873=ORIENTED_EDGE('',*,*,#4444,.F.);
#5874=ORIENTED_EDGE('',*,*,#4445,.T.);
#5875=ORIENTED_EDGE('',*,*,#4422,.T.);
#5876=ORIENTED_EDGE('',*,*,#4425,.T.);
#5877=ORIENTED_EDGE('',*,*,#4439,.T.);
#5878=ORIENTED_EDGE('',*,*,#4434,.F.);
#5879=ORIENTED_EDGE('',*,*,#4446,.F.);
#5880=ORIENTED_EDGE('',*,*,#4441,.T.);
#5881=ORIENTED_EDGE('',*,*,#4442,.T.);
#5882=ORIENTED_EDGE('',*,*,#4446,.T.);
#5883=ORIENTED_EDGE('',*,*,#4433,.T.);
#5884=ORIENTED_EDGE('',*,*,#4447,.T.);
#5885=ORIENTED_EDGE('',*,*,#4448,.T.);
#5886=ORIENTED_EDGE('',*,*,#4449,.T.);
#5887=ORIENTED_EDGE('',*,*,#4448,.F.);
#5888=ORIENTED_EDGE('',*,*,#4450,.F.);
#5889=ORIENTED_EDGE('',*,*,#4451,.T.);
#5890=ORIENTED_EDGE('',*,*,#4429,.F.);
#5891=ORIENTED_EDGE('',*,*,#4451,.F.);
#5892=ORIENTED_EDGE('',*,*,#4452,.F.);
#5893=ORIENTED_EDGE('',*,*,#4453,.F.);
#5894=ORIENTED_EDGE('',*,*,#4454,.F.);
#5895=ORIENTED_EDGE('',*,*,#4447,.F.);
#5896=ORIENTED_EDGE('',*,*,#4432,.F.);
#5897=ORIENTED_EDGE('',*,*,#4455,.F.);
#5898=ORIENTED_EDGE('',*,*,#4452,.T.);
#5899=ORIENTED_EDGE('',*,*,#4450,.T.);
#5900=ORIENTED_EDGE('',*,*,#4449,.F.);
#5901=ORIENTED_EDGE('',*,*,#4454,.T.);
#5902=ORIENTED_EDGE('',*,*,#4456,.F.);
#5903=ORIENTED_EDGE('',*,*,#4443,.F.);
#5904=ORIENTED_EDGE('',*,*,#4431,.T.);
#5905=ORIENTED_EDGE('',*,*,#4457,.T.);
#5906=ORIENTED_EDGE('',*,*,#4444,.T.);
#5907=ORIENTED_EDGE('',*,*,#4456,.T.);
#5908=ORIENTED_EDGE('',*,*,#4453,.T.);
#5909=ORIENTED_EDGE('',*,*,#4455,.T.);
#5910=ORIENTED_EDGE('',*,*,#4419,.T.);
#5911=ORIENTED_EDGE('',*,*,#4445,.F.);
#5912=ORIENTED_EDGE('',*,*,#4457,.F.);
#5913=ORIENTED_EDGE('',*,*,#4430,.T.);
#6635=CYLINDRICAL_SURFACE('',#7911,0.2117);
#6912=ADVANCED_FACE('',(#1070),#706,.F.);
#6913=ADVANCED_FACE('',(#1071),#707,.T.);
#6914=ADVANCED_FACE('',(#1072,#495),#708,.T.);
#6915=ADVANCED_FACE('',(#1073),#709,.T.);
#6916=ADVANCED_FACE('',(#1074),#710,.T.);
#6917=ADVANCED_FACE('',(#1075),#711,.F.);
#6918=ADVANCED_FACE('',(#1076),#712,.T.);
#6919=ADVANCED_FACE('',(#1077),#713,.T.);
#6920=ADVANCED_FACE('',(#1078),#714,.T.);
#6921=ADVANCED_FACE('',(#1079),#6635,.F.);
#6922=ADVANCED_FACE('',(#1080),#715,.F.);
#6923=ADVANCED_FACE('',(#1081),#716,.F.);
#6924=ADVANCED_FACE('',(#1082),#717,.T.);
#6925=ADVANCED_FACE('',(#1083),#718,.T.);
#7096=CLOSED_SHELL('',(#6912,#6913,#6914,#6915,#6916,#6917,#6918,#6919,
#6920,#6921,#6922,#6923,#6924,#6925));
#7899=AXIS2_PLACEMENT_3D('',#14114,#9411,#9412);
#7900=AXIS2_PLACEMENT_3D('',#14115,#9413,#9414);
#7901=AXIS2_PLACEMENT_3D('',#14124,#9419,#9420);
#7902=AXIS2_PLACEMENT_3D('',#14130,#9424,#9425);
#7903=AXIS2_PLACEMENT_3D('',#14137,#9429,#9430);
#7904=AXIS2_PLACEMENT_3D('',#14138,#9431,#9432);
#7905=AXIS2_PLACEMENT_3D('',#14152,#9440,#9441);
#7906=AXIS2_PLACEMENT_3D('',#14156,#9444,#9445);
#7907=AXIS2_PLACEMENT_3D('',#14160,#9448,#9449);
#7908=AXIS2_PLACEMENT_3D('',#14170,#9455,#9456);
#7909=AXIS2_PLACEMENT_3D('',#14172,#9458,#9459);
#7910=AXIS2_PLACEMENT_3D('',#14176,#9461,#9462);
#7911=AXIS2_PLACEMENT_3D('',#14178,#9464,#9465);
#7912=AXIS2_PLACEMENT_3D('',#14180,#9466,#9467);
#7913=AXIS2_PLACEMENT_3D('',#14183,#9469,#9470);
#7914=AXIS2_PLACEMENT_3D('',#14185,#9471,#9472);
#7915=AXIS2_PLACEMENT_3D('',#14186,#9473,#9474);
#7916=AXIS2_PLACEMENT_3D('',#14187,#9475,#9476);
#7917=AXIS2_PLACEMENT_3D('',#14189,#9478,#9479);
#7918=AXIS2_PLACEMENT_3D('',#14191,#9481,#9482);
#7919=AXIS2_PLACEMENT_3D('',#14193,#9484,#9485);
#9411=DIRECTION('axis',(0.,0.,1.));
#9412=DIRECTION('refdir',(1.,0.,0.));
#9413=DIRECTION('center_axis',(0.,0.,1.));
#9414=DIRECTION('ref_axis',(1.,0.,0.));
#9415=DIRECTION('',(1.,0.,0.));
#9416=DIRECTION('',(0.,-1.,0.));
#9417=DIRECTION('',(-1.,0.,0.));
#9418=DIRECTION('',(0.,1.,0.));
#9419=DIRECTION('center_axis',(0.,1.,0.));
#9420=DIRECTION('ref_axis',(-1.,0.,0.));
#9421=DIRECTION('',(0.,0.,1.));
#9422=DIRECTION('',(-1.,0.,0.));
#9423=DIRECTION('',(0.,0.,1.));
#9424=DIRECTION('center_axis',(0.,0.,1.));
#9425=DIRECTION('ref_axis',(1.,0.,0.));
#9426=DIRECTION('',(0.,-1.,0.));
#9427=DIRECTION('',(1.,0.,0.));
#9428=DIRECTION('',(0.,1.,0.));
#9429=DIRECTION('center_axis',(0.,0.,-1.));
#9430=DIRECTION('ref_axis',(1.,0.,0.));
#9431=DIRECTION('center_axis',(-1.,0.,0.));
#9432=DIRECTION('ref_axis',(0.,-1.,0.));
#9433=DIRECTION('',(0.,0.,1.));
#9434=DIRECTION('',(0.,0.707106781186548,0.707106781186548));
#9435=DIRECTION('',(0.,-1.,0.));
#9436=DIRECTION('',(0.,0.707106781186548,-0.707106781186548));
#9437=DIRECTION('',(0.,0.,1.));
#9438=DIRECTION('',(0.,-1.,0.));
#9439=DIRECTION('',(0.,0.,1.));
#9440=DIRECTION('center_axis',(0.,-1.,0.));
#9441=DIRECTION('ref_axis',(1.,0.,0.));
#9442=DIRECTION('',(1.,0.,0.));
#9443=DIRECTION('',(0.,0.,1.));
#9444=DIRECTION('center_axis',(0.,0.,1.));
#9445=DIRECTION('ref_axis',(1.,0.,0.));
#9446=DIRECTION('',(-1.,0.,0.));
#9447=DIRECTION('',(0.,1.,0.));
#9448=DIRECTION('center_axis',(1.,0.,0.));
#9449=DIRECTION('ref_axis',(0.,1.,0.));
#9450=DIRECTION('',(0.,0.,1.));
#9451=DIRECTION('',(0.,-0.707106781186548,0.707106781186548));
#9452=DIRECTION('',(0.,1.,0.));
#9453=DIRECTION('',(0.,-0.707106781186548,-0.707106781186548));
#9454=DIRECTION('',(0.,0.,1.));
#9455=DIRECTION('center_axis',(0.,-1.,0.));
#9456=DIRECTION('ref_axis',(1.,0.,0.));
#9457=DIRECTION('',(-1.,0.,0.));
#9458=DIRECTION('center_axis',(0.,-0.707106781186548,-0.707106781186548));
#9459=DIRECTION('ref_axis',(-1.,0.,0.));
#9460=DIRECTION('',(1.,0.,0.));
#9461=DIRECTION('center_axis',(0.,0.707106781186548,0.707106781186548));
#9462=DIRECTION('ref_axis',(0.,0.707106781186547,-0.707106781186547));
#9463=DIRECTION('',(1.,0.,0.));
#9464=DIRECTION('center_axis',(0.,0.,1.));
#9465=DIRECTION('ref_axis',(1.,0.,0.));
#9466=DIRECTION('center_axis',(0.,0.,-1.));
#9467=DIRECTION('ref_axis',(1.,0.,0.));
#9468=DIRECTION('',(0.,0.,1.));
#9469=DIRECTION('center_axis',(0.,0.,-1.));
#9470=DIRECTION('ref_axis',(1.,0.,0.));
#9471=DIRECTION('center_axis',(0.,-0.707106781186548,0.707106781186548));
#9472=DIRECTION('ref_axis',(0.,0.707106781186547,0.707106781186547));
#9473=DIRECTION('center_axis',(0.,0.,-1.));
#9474=DIRECTION('ref_axis',(1.,0.,0.));
#9475=DIRECTION('center_axis',(0.,0.,1.));
#9476=DIRECTION('ref_axis',(1.,0.,0.));
#9477=DIRECTION('',(-1.,0.,0.));
#9478=DIRECTION('center_axis',(0.,0.,1.));
#9479=DIRECTION('ref_axis',(1.,0.,0.));
#9480=DIRECTION('',(-1.,0.,0.));
#9481=DIRECTION('center_axis',(0.,0.707106781186548,-0.707106781186548));
#9482=DIRECTION('ref_axis',(-1.,0.,0.));
#9483=DIRECTION('',(1.,0.,0.));
#9484=DIRECTION('center_axis',(0.,1.,0.));
#9485=DIRECTION('ref_axis',(-1.,0.,0.));
#14114=CARTESIAN_POINT('',(0.,0.,0.));
#14115=CARTESIAN_POINT('Origin',(0.,0.395,0.25));
#14116=CARTESIAN_POINT('',(-0.5,0.3,0.25));
#14117=CARTESIAN_POINT('',(0.5,0.3,0.25));
#14118=CARTESIAN_POINT('',(0.25,0.3,0.25));
#14119=CARTESIAN_POINT('',(-0.5,0.5,0.25));
#14120=CARTESIAN_POINT('',(-0.5,0.5,0.25));
#14121=CARTESIAN_POINT('',(0.5,0.5,0.25));
#14122=CARTESIAN_POINT('',(0.5,0.5,0.25));
#14123=CARTESIAN_POINT('',(0.5,0.29,0.25));
#14124=CARTESIAN_POINT('Origin',(0.5,0.5,0.25));
#14125=CARTESIAN_POINT('',(-0.5,0.5,0.4));
#14126=CARTESIAN_POINT('',(-0.5,0.5,0.25));
#14127=CARTESIAN_POINT('',(0.5,0.5,0.4));
#14128=CARTESIAN_POINT('',(0.5,0.5,0.4));
#14129=CARTESIAN_POINT('',(0.5,0.5,0.25));
#14130=CARTESIAN_POINT('Origin',(0.,0.,0.4));
#14131=CARTESIAN_POINT('',(-0.5,-0.5,0.4));
#14132=CARTESIAN_POINT('',(-0.5,0.5,0.4));
#14133=CARTESIAN_POINT('',(0.5,-0.5,0.4));
#14134=CARTESIAN_POINT('',(-0.5,-0.5,0.4));
#14135=CARTESIAN_POINT('',(0.5,-0.3,0.4));
#14136=CARTESIAN_POINT('',(-0.2117,2.59257727379495E-17,0.4));
#14137=CARTESIAN_POINT('Origin',(0.,0.,0.4));
#14138=CARTESIAN_POINT('Origin',(-0.5,0.3,0.));
#14139=CARTESIAN_POINT('',(-0.5,0.3,0.15));
#14140=CARTESIAN_POINT('',(-0.5,0.3,0.));
#14141=CARTESIAN_POINT('',(-0.5,0.15,0.));
#14142=CARTESIAN_POINT('',(-0.5,0.225,0.075));
#14143=CARTESIAN_POINT('',(-0.5,-0.15,0.));
#14144=CARTESIAN_POINT('',(-0.5,0.3,0.));
#14145=CARTESIAN_POINT('',(-0.5,-0.3,0.15));
#14146=CARTESIAN_POINT('',(-0.5,-0.075,-0.075));
#14147=CARTESIAN_POINT('',(-0.5,-0.3,0.25));
#14148=CARTESIAN_POINT('',(-0.5,-0.3,0.));
#14149=CARTESIAN_POINT('',(-0.5,-0.5,0.25));
#14150=CARTESIAN_POINT('',(-0.5,-0.29,0.25));
#14151=CARTESIAN_POINT('',(-0.5,-0.5,0.25));
#14152=CARTESIAN_POINT('Origin',(-0.5,-0.5,0.25));
#14153=CARTESIAN_POINT('',(0.5,-0.5,0.25));
#14154=CARTESIAN_POINT('',(-0.5,-0.5,0.25));
#14155=CARTESIAN_POINT('',(0.5,-0.5,0.25));
#14156=CARTESIAN_POINT('Origin',(0.,-0.395,0.25));
#14157=CARTESIAN_POINT('',(0.5,-0.3,0.25));
#14158=CARTESIAN_POINT('',(-0.25,-0.3,0.25));
#14159=CARTESIAN_POINT('',(0.5,-0.5,0.25));
#14160=CARTESIAN_POINT('Origin',(0.5,-0.3,0.));
#14161=CARTESIAN_POINT('',(0.5,-0.3,0.15));
#14162=CARTESIAN_POINT('',(0.5,-0.3,0.));
#14163=CARTESIAN_POINT('',(0.5,-0.15,0.));
#14164=CARTESIAN_POINT('',(0.5,-0.225,0.075));
#14165=CARTESIAN_POINT('',(0.5,0.15,0.));
#14166=CARTESIAN_POINT('',(0.5,-0.3,0.));
#14167=CARTESIAN_POINT('',(0.5,0.3,0.15));
#14168=CARTESIAN_POINT('',(0.5,0.075,-0.075));
#14169=CARTESIAN_POINT('',(0.5,0.3,0.));
#14170=CARTESIAN_POINT('Origin',(-0.5,-0.3,0.));
#14171=CARTESIAN_POINT('',(-0.25,-0.3,0.15));
#14172=CARTESIAN_POINT('Origin',(-0.25,-0.225,0.075));
#14173=CARTESIAN_POINT('',(-0.149388386429468,-0.15,0.));
#14174=CARTESIAN_POINT('',(-0.25,-0.15,0.));
#14175=CARTESIAN_POINT('',(0.149388386429468,-0.15,0.));
#14176=CARTESIAN_POINT('Origin',(0.,0.,-0.15));
#14177=CARTESIAN_POINT('',(-0.25,-0.15,0.));
#14178=CARTESIAN_POINT('Origin',(0.,0.,-0.1));
#14179=CARTESIAN_POINT('',(-0.2117,-2.59257727379495E-17,0.));
#14180=CARTESIAN_POINT('Origin',(0.,0.,0.));
#14181=CARTESIAN_POINT('',(-0.2117,-2.59257727379495E-17,-0.1));
#14182=CARTESIAN_POINT('',(-0.149388386429468,0.15,0.));
#14183=CARTESIAN_POINT('Origin',(0.,0.,0.));
#14184=CARTESIAN_POINT('',(0.149388386429468,0.15,0.));
#14185=CARTESIAN_POINT('Origin',(0.,0.,-0.15));
#14186=CARTESIAN_POINT('Origin',(0.,0.,0.));
#14187=CARTESIAN_POINT('Origin',(0.,0.,0.));
#14188=CARTESIAN_POINT('',(0.25,0.15,0.));
#14189=CARTESIAN_POINT('Origin',(0.,0.,0.));
#14190=CARTESIAN_POINT('',(0.25,0.15,0.));
#14191=CARTESIAN_POINT('Origin',(0.25,0.225,0.075));
#14192=CARTESIAN_POINT('',(0.25,0.3,0.15));
#14193=CARTESIAN_POINT('Origin',(0.5,0.3,0.));
#14984=UNCERTAINTY_MEASURE_WITH_UNIT(LENGTH_MEASURE(0.001),#15041,
'DISTANCE_ACCURACY_VALUE',
'Maximum model space distance between geometric entities at asserted c
onnectivities');
#15000=UNCERTAINTY_MEASURE_WITH_UNIT(LENGTH_MEASURE(0.001),#15041,
'DISTANCE_ACCURACY_VALUE',
'Maximum model space distance between geometric entities at asserted c
onnectivities');
#15024=(
GEOMETRIC_REPRESENTATION_CONTEXT(3)
GLOBAL_UNCERTAINTY_ASSIGNED_CONTEXT((#14984))
GLOBAL_UNIT_ASSIGNED_CONTEXT((#15041,#15043,#15044))
REPRESENTATION_CONTEXT('','3D')
);
#15040=(
GEOMETRIC_REPRESENTATION_CONTEXT(3)
GLOBAL_UNCERTAINTY_ASSIGNED_CONTEXT((#15000))
GLOBAL_UNIT_ASSIGNED_CONTEXT((#15041,#15043,#15044))
REPRESENTATION_CONTEXT('','3D')
);
#15041=(
LENGTH_UNIT()
NAMED_UNIT(*)
SI_UNIT(.CENTI.,.METRE.)
);
#15043=(
NAMED_UNIT(*)
PLANE_ANGLE_UNIT()
SI_UNIT($,.RADIAN.)
);
#15044=(
NAMED_UNIT(*)
SI_UNIT($,.STERADIAN.)
SOLID_ANGLE_UNIT()
);
#15068=SHAPE_DEFINITION_REPRESENTATION(#15107,#15205);
#15107=PRODUCT_DEFINITION_SHAPE('',$,#15245);
#15205=SHAPE_REPRESENTATION('',(#7899),#15024);
#15221=PRODUCT_DEFINITION_CONTEXT('part definition',#15340,'design');
#15245=PRODUCT_DEFINITION('Captive slot nut','Captive slot nut',#15284,
#15221);
#15284=PRODUCT_DEFINITION_FORMATION('',$,#15365);
#15340=APPLICATION_CONTEXT(
'Core Data for Automotive Mechanical Design Process');
#15341=PRODUCT_CONTEXT('part definition',#15340,'mechanical');
#15365=PRODUCT('Captive slot nut','Captive slot nut','Captive slot nut',
(#15341));
#15458=COLOUR_RGB('Black',0.12,0.14,0.17);
#15459=FILL_AREA_STYLE_COLOUR('',#15458);
#15460=FILL_AREA_STYLE('',(#15459));
#15461=SURFACE_STYLE_FILL_AREA(#15460);
#15462=SURFACE_SIDE_STYLE('',(#15461));
#15463=SURFACE_STYLE_USAGE(.BOTH.,#15462);
#15464=PRESENTATION_STYLE_ASSIGNMENT((#15463));
ENDSEC;
END-ISO-10303-21;
